ISO-10303-21;
HEADER;
/* Generated by software containing ST-Developer
 * from STEP Tools, Inc. (www.steptools.com) 
 */

FILE_DESCRIPTION(
/* description */ ('PAT-082'),
/* implementation_level */ '2;1');

FILE_NAME(
/* name */ 'Cap Screw - M4x16.step',
/* time_stamp */ '2026-10-29T20:16:13-07:00',
/* author */ (''),
/* organization */ (''),
/* preprocessor_version */ 'ST-DEVELOPER v20.2',
/* originating_system */ 'Autodesk Translation Framework v15.17.0.0',
/* authorisation */ '');

FILE_SCHEMA (('AUTOMOTIVE_DESIGN { 1 0 10303 214 3 1 1 }'));
ENDSEC;

DATA;
#10=MECHANICAL_DESIGN_GEOMETRIC_PRESENTATION_REPRESENTATION('',(#261),#8266);
#172=CONICAL_SURFACE('',#5298,0.325,0.785398163397448);
#173=CONICAL_SURFACE('',#5302,0.335,0.785398163397448);
#174=CONICAL_SURFACE('',#5306,0.21,0.463647609000806);
#175=CONICAL_SURFACE('',#5310,0.18,0.785398163397448);
#180=ORIENTED_CLOSED_SHELL('',*,#4603,.F.);
#183=BREP_WITH_VOIDS('Body1',#4602,(#180));
#217=SHAPE_REPRESENTATION_RELATIONSHIP('SRR','None',#8380,#239);
#239=ADVANCED_BREP_SHAPE_REPRESENTATION('',(#183),#8264);
#261=STYLED_ITEM('',(#8544),#183);
#403=FACE_BOUND('',#1205,.T.);
#550=PLANE('',#5296);
#551=PLANE('',#5304);
#552=PLANE('',#5312);
#553=PLANE('',#5313);
#554=PLANE('',#5314);
#555=PLANE('',#5315);
#556=PLANE('',#5316);
#557=PLANE('',#5317);
#558=PLANE('',#5318);
#559=PLANE('',#5319);
#560=PLANE('',#5320);
#809=FACE_OUTER_BOUND('',#1200,.T.);
#810=FACE_OUTER_BOUND('',#1201,.T.);
#811=FACE_OUTER_BOUND('',#1202,.T.);
#812=FACE_OUTER_BOUND('',#1203,.T.);
#813=FACE_OUTER_BOUND('',#1204,.T.);
#814=FACE_OUTER_BOUND('',#1206,.T.);
#815=FACE_OUTER_BOUND('',#1207,.T.);
#816=FACE_OUTER_BOUND('',#1208,.T.);
#817=FACE_OUTER_BOUND('',#1209,.T.);
#818=FACE_OUTER_BOUND('',#1210,.T.);
#819=FACE_OUTER_BOUND('',#1211,.T.);
#820=FACE_OUTER_BOUND('',#1212,.T.);
#821=FACE_OUTER_BOUND('',#1213,.T.);
#822=FACE_OUTER_BOUND('',#1214,.T.);
#823=FACE_OUTER_BOUND('',#1215,.T.);
#824=FACE_OUTER_BOUND('',#1216,.T.);
#825=FACE_OUTER_BOUND('',#1217,.T.);
#1200=EDGE_LOOP('',(#4096));
#1201=EDGE_LOOP('',(#4097,#4098,#4099,#4100));
#1202=EDGE_LOOP('',(#4101,#4102,#4103,#4104));
#1203=EDGE_LOOP('',(#4105,#4106,#4107,#4108));
#1204=EDGE_LOOP('',(#4109));
#1205=EDGE_LOOP('',(#4110));
#1206=EDGE_LOOP('',(#4111,#4112,#4113,#4114));
#1207=EDGE_LOOP('',(#4115,#4116,#4117,#4118));
#1208=EDGE_LOOP('',(#4119,#4120,#4121,#4122));
#1209=EDGE_LOOP('',(#4123));
#1210=EDGE_LOOP('',(#4124,#4125,#4126,#4127));
#1211=EDGE_LOOP('',(#4128,#4129,#4130,#4131));
#1212=EDGE_LOOP('',(#4132,#4133,#4134,#4135));
#1213=EDGE_LOOP('',(#4136,#4137,#4138,#4139));
#1214=EDGE_LOOP('',(#4140,#4141,#4142,#4143));
#1215=EDGE_LOOP('',(#4144,#4145,#4146,#4147));
#1216=EDGE_LOOP('',(#4148,#4149,#4150,#4151,#4152,#4153));
#1217=EDGE_LOOP('',(#4154,#4155,#4156,#4157,#4158,#4159));
#1543=LINE('',#8051,#1898);
#1544=LINE('',#8055,#1899);
#1545=LINE('',#8059,#1900);
#1546=LINE('',#8066,#1901);
#1547=LINE('',#8070,#1902);
#1548=LINE('',#8074,#1903);
#1549=LINE('',#8079,#1904);
#1550=LINE('',#8081,#1905);
#1551=LINE('',#8083,#1906);
#1552=LINE('',#8084,#1907);
#1553=LINE('',#8087,#1908);
#1554=LINE('',#8089,#1909);
#1555=LINE('',#8090,#1910);
#1556=LINE('',#8093,#1911);
#1557=LINE('',#8095,#1912);
#1558=LINE('',#8096,#1913);
#1559=LINE('',#8099,#1914);
#1560=LINE('',#8101,#1915);
#1561=LINE('',#8102,#1916);
#1562=LINE('',#8105,#1917);
#1563=LINE('',#8107,#1918);
#1564=LINE('',#8108,#1919);
#1565=LINE('',#8110,#1920);
#1566=LINE('',#8111,#1921);
#1898=VECTOR('',#6592,0.325);
#1899=VECTOR('',#6597,0.35);
#1900=VECTOR('',#6602,0.335);
#1901=VECTOR('',#6611,0.21);
#1902=VECTOR('',#6616,0.2);
#1903=VECTOR('',#6621,0.18);
#1904=VECTOR('',#6626,1.);
#1905=VECTOR('',#6627,1.);
#1906=VECTOR('',#6628,1.);
#1907=VECTOR('',#6629,1.);
#1908=VECTOR('',#6632,1.);
#1909=VECTOR('',#6633,1.);
#1910=VECTOR('',#6634,1.);
#1911=VECTOR('',#6637,1.);
#1912=VECTOR('',#6638,1.);
#1913=VECTOR('',#6639,1.);
#1914=VECTOR('',#6642,1.);
#1915=VECTOR('',#6643,1.);
#1916=VECTOR('',#6644,1.);
#1917=VECTOR('',#6647,1.);
#1918=VECTOR('',#6648,1.);
#1919=VECTOR('',#6649,1.);
#1920=VECTOR('',#6652,1.);
#1921=VECTOR('',#6653,1.);
#2130=CIRCLE('',#5297,0.3);
#2131=CIRCLE('',#5299,0.35);
#2132=CIRCLE('',#5301,0.35);
#2133=CIRCLE('',#5303,0.32);
#2134=CIRCLE('',#5305,0.22);
#2135=CIRCLE('',#5307,0.1954);
#2136=CIRCLE('',#5309,0.1954);
#2137=CIRCLE('',#5311,0.16);
#2480=VERTEX_POINT('',#8046);
#2481=VERTEX_POINT('',#8049);
#2482=VERTEX_POINT('',#8053);
#2483=VERTEX_POINT('',#8057);
#2484=VERTEX_POINT('',#8061);
#2485=VERTEX_POINT('',#8064);
#2486=VERTEX_POINT('',#8068);
#2487=VERTEX_POINT('',#8072);
#2488=VERTEX_POINT('',#8077);
#2489=VERTEX_POINT('',#8078);
#2490=VERTEX_POINT('',#8080);
#2491=VERTEX_POINT('',#8082);
#2492=VERTEX_POINT('',#8086);
#2493=VERTEX_POINT('',#8088);
#2494=VERTEX_POINT('',#8092);
#2495=VERTEX_POINT('',#8094);
#2496=VERTEX_POINT('',#8098);
#2497=VERTEX_POINT('',#8100);
#2498=VERTEX_POINT('',#8104);
#2499=VERTEX_POINT('',#8106);
#3024=EDGE_CURVE('',#2480,#2480,#2130,.T.);
#3025=EDGE_CURVE('',#2481,#2481,#2131,.T.);
#3026=EDGE_CURVE('',#2481,#2480,#1543,.T.);
#3027=EDGE_CURVE('',#2482,#2482,#2132,.T.);
#3028=EDGE_CURVE('',#2482,#2481,#1544,.T.);
#3029=EDGE_CURVE('',#2483,#2483,#2133,.T.);
#3030=EDGE_CURVE('',#2483,#2482,#1545,.T.);
#3031=EDGE_CURVE('',#2484,#2484,#2134,.T.);
#3032=EDGE_CURVE('',#2485,#2485,#2135,.F.);
#3033=EDGE_CURVE('',#2485,#2484,#1546,.T.);
#3034=EDGE_CURVE('',#2486,#2486,#2136,.F.);
#3035=EDGE_CURVE('',#2486,#2485,#1547,.T.);
#3036=EDGE_CURVE('',#2487,#2487,#2137,.T.);
#3037=EDGE_CURVE('',#2487,#2486,#1548,.T.);
#3038=EDGE_CURVE('',#2488,#2489,#1549,.T.);
#3039=EDGE_CURVE('',#2489,#2490,#1550,.T.);
#3040=EDGE_CURVE('',#2490,#2491,#1551,.T.);
#3041=EDGE_CURVE('',#2488,#2491,#1552,.T.);
#3042=EDGE_CURVE('',#2489,#2492,#1553,.T.);
#3043=EDGE_CURVE('',#2492,#2493,#1554,.T.);
#3044=EDGE_CURVE('',#2493,#2490,#1555,.T.);
#3045=EDGE_CURVE('',#2492,#2494,#1556,.T.);
#3046=EDGE_CURVE('',#2494,#2495,#1557,.T.);
#3047=EDGE_CURVE('',#2495,#2493,#1558,.T.);
#3048=EDGE_CURVE('',#2494,#2496,#1559,.T.);
#3049=EDGE_CURVE('',#2496,#2497,#1560,.T.);
#3050=EDGE_CURVE('',#2497,#2495,#1561,.T.);
#3051=EDGE_CURVE('',#2496,#2498,#1562,.T.);
#3052=EDGE_CURVE('',#2498,#2499,#1563,.T.);
#3053=EDGE_CURVE('',#2499,#2497,#1564,.T.);
#3054=EDGE_CURVE('',#2498,#2488,#1565,.T.);
#3055=EDGE_CURVE('',#2491,#2499,#1566,.T.);
#4096=ORIENTED_EDGE('',*,*,#3024,.F.);
#4097=ORIENTED_EDGE('',*,*,#3025,.F.);
#4098=ORIENTED_EDGE('',*,*,#3026,.T.);
#4099=ORIENTED_EDGE('',*,*,#3024,.T.);
#4100=ORIENTED_EDGE('',*,*,#3026,.F.);
#4101=ORIENTED_EDGE('',*,*,#3027,.F.);
#4102=ORIENTED_EDGE('',*,*,#3028,.T.);
#4103=ORIENTED_EDGE('',*,*,#3025,.T.);
#4104=ORIENTED_EDGE('',*,*,#3028,.F.);
#4105=ORIENTED_EDGE('',*,*,#3029,.F.);
#4106=ORIENTED_EDGE('',*,*,#3030,.T.);
#4107=ORIENTED_EDGE('',*,*,#3027,.T.);
#4108=ORIENTED_EDGE('',*,*,#3030,.F.);
#4109=ORIENTED_EDGE('',*,*,#3029,.T.);
#4110=ORIENTED_EDGE('',*,*,#3031,.F.);
#4111=ORIENTED_EDGE('',*,*,#3032,.F.);
#4112=ORIENTED_EDGE('',*,*,#3033,.T.);
#4113=ORIENTED_EDGE('',*,*,#3031,.T.);
#4114=ORIENTED_EDGE('',*,*,#3033,.F.);
#4115=ORIENTED_EDGE('',*,*,#3034,.F.);
#4116=ORIENTED_EDGE('',*,*,#3035,.T.);
#4117=ORIENTED_EDGE('',*,*,#3032,.T.);
#4118=ORIENTED_EDGE('',*,*,#3035,.F.);
#4119=ORIENTED_EDGE('',*,*,#3036,.F.);
#4120=ORIENTED_EDGE('',*,*,#3037,.T.);
#4121=ORIENTED_EDGE('',*,*,#3034,.T.);
#4122=ORIENTED_EDGE('',*,*,#3037,.F.);
#4123=ORIENTED_EDGE('',*,*,#3036,.T.);
#4124=ORIENTED_EDGE('',*,*,#3038,.T.);
#4125=ORIENTED_EDGE('',*,*,#3039,.T.);
#4126=ORIENTED_EDGE('',*,*,#3040,.T.);
#4127=ORIENTED_EDGE('',*,*,#3041,.F.);
#4128=ORIENTED_EDGE('',*,*,#3042,.T.);
#4129=ORIENTED_EDGE('',*,*,#3043,.T.);
#4130=ORIENTED_EDGE('',*,*,#3044,.T.);
#4131=ORIENTED_EDGE('',*,*,#3039,.F.);
#4132=ORIENTED_EDGE('',*,*,#3045,.T.);
#4133=ORIENTED_EDGE('',*,*,#3046,.T.);
#4134=ORIENTED_EDGE('',*,*,#3047,.T.);
#4135=ORIENTED_EDGE('',*,*,#3043,.F.);
#4136=ORIENTED_EDGE('',*,*,#3048,.T.);
#4137=ORIENTED_EDGE('',*,*,#3049,.T.);
#4138=ORIENTED_EDGE('',*,*,#3050,.T.);
#4139=ORIENTED_EDGE('',*,*,#3046,.F.);
#4140=ORIENTED_EDGE('',*,*,#3051,.T.);
#4141=ORIENTED_EDGE('',*,*,#3052,.T.);
#4142=ORIENTED_EDGE('',*,*,#3053,.T.);
#4143=ORIENTED_EDGE('',*,*,#3049,.F.);
#4144=ORIENTED_EDGE('',*,*,#3054,.T.);
#4145=ORIENTED_EDGE('',*,*,#3041,.T.);
#4146=ORIENTED_EDGE('',*,*,#3055,.T.);
#4147=ORIENTED_EDGE('',*,*,#3052,.F.);
#4148=ORIENTED_EDGE('',*,*,#3054,.F.);
#4149=ORIENTED_EDGE('',*,*,#3051,.F.);
#4150=ORIENTED_EDGE('',*,*,#3048,.F.);
#4151=ORIENTED_EDGE('',*,*,#3045,.F.);
#4152=ORIENTED_EDGE('',*,*,#3042,.F.);
#4153=ORIENTED_EDGE('',*,*,#3038,.F.);
#4154=ORIENTED_EDGE('',*,*,#3055,.F.);
#4155=ORIENTED_EDGE('',*,*,#3040,.F.);
#4156=ORIENTED_EDGE('',*,*,#3044,.F.);
#4157=ORIENTED_EDGE('',*,*,#3047,.F.);
#4158=ORIENTED_EDGE('',*,*,#3050,.F.);
#4159=ORIENTED_EDGE('',*,*,#3053,.F.);
#4307=CYLINDRICAL_SURFACE('',#5300,0.35);
#4308=CYLINDRICAL_SURFACE('',#5308,0.1954);
#4548=ADVANCED_FACE('',(#809),#550,.T.);
#4549=ADVANCED_FACE('',(#810),#172,.T.);
#4550=ADVANCED_FACE('',(#811),#4307,.T.);
#4551=ADVANCED_FACE('',(#812),#173,.T.);
#4552=ADVANCED_FACE('',(#813,#403),#551,.T.);
#4553=ADVANCED_FACE('',(#814),#174,.T.);
#4554=ADVANCED_FACE('',(#815),#4308,.T.);
#4555=ADVANCED_FACE('',(#816),#175,.T.);
#4556=ADVANCED_FACE('',(#817),#552,.T.);
#4557=ADVANCED_FACE('',(#818),#553,.F.);
#4558=ADVANCED_FACE('',(#819),#554,.F.);
#4559=ADVANCED_FACE('',(#820),#555,.F.);
#4560=ADVANCED_FACE('',(#821),#556,.F.);
#4561=ADVANCED_FACE('',(#822),#557,.F.);
#4562=ADVANCED_FACE('',(#823),#558,.F.);
#4563=ADVANCED_FACE('',(#824),#559,.F.);
#4564=ADVANCED_FACE('',(#825),#560,.F.);
#4602=CLOSED_SHELL('',(#4548,#4549,#4550,#4551,#4552,#4553,#4554,#4555,
#4556));
#4603=CLOSED_SHELL('',(#4557,#4558,#4559,#4560,#4561,#4562,#4563,#4564));
#5295=AXIS2_PLACEMENT_3D('',#8044,#6582,#6583);
#5296=AXIS2_PLACEMENT_3D('',#8045,#6584,#6585);
#5297=AXIS2_PLACEMENT_3D('',#8047,#6586,#6587);
#5298=AXIS2_PLACEMENT_3D('',#8048,#6588,#6589);
#5299=AXIS2_PLACEMENT_3D('',#8050,#6590,#6591);
#5300=AXIS2_PLACEMENT_3D('',#8052,#6593,#6594);
#5301=AXIS2_PLACEMENT_3D('',#8054,#6595,#6596);
#5302=AXIS2_PLACEMENT_3D('',#8056,#6598,#6599);
#5303=AXIS2_PLACEMENT_3D('',#8058,#6600,#6601);
#5304=AXIS2_PLACEMENT_3D('',#8060,#6603,#6604);
#5305=AXIS2_PLACEMENT_3D('',#8062,#6605,#6606);
#5306=AXIS2_PLACEMENT_3D('',#8063,#6607,#6608);
#5307=AXIS2_PLACEMENT_3D('',#8065,#6609,#6610);
#5308=AXIS2_PLACEMENT_3D('',#8067,#6612,#6613);
#5309=AXIS2_PLACEMENT_3D('',#8069,#6614,#6615);
#5310=AXIS2_PLACEMENT_3D('',#8071,#6617,#6618);
#5311=AXIS2_PLACEMENT_3D('',#8073,#6619,#6620);
#5312=AXIS2_PLACEMENT_3D('',#8075,#6622,#6623);
#5313=AXIS2_PLACEMENT_3D('',#8076,#6624,#6625);
#5314=AXIS2_PLACEMENT_3D('',#8085,#6630,#6631);
#5315=AXIS2_PLACEMENT_3D('',#8091,#6635,#6636);
#5316=AXIS2_PLACEMENT_3D('',#8097,#6640,#6641);
#5317=AXIS2_PLACEMENT_3D('',#8103,#6645,#6646);
#5318=AXIS2_PLACEMENT_3D('',#8109,#6650,#6651);
#5319=AXIS2_PLACEMENT_3D('',#8112,#6654,#6655);
#5320=AXIS2_PLACEMENT_3D('',#8113,#6656,#6657);
#6582=DIRECTION('axis',(0.,0.,1.));
#6583=DIRECTION('refdir',(1.,0.,0.));
#6584=DIRECTION('center_axis',(0.,1.,0.));
#6585=DIRECTION('ref_axis',(0.,0.,1.));
#6586=DIRECTION('center_axis',(0.,-1.,0.));
#6587=DIRECTION('ref_axis',(1.,0.,0.));
#6588=DIRECTION('center_axis',(0.,-1.,0.));
#6589=DIRECTION('ref_axis',(1.,0.,0.));
#6590=DIRECTION('center_axis',(0.,-1.,0.));
#6591=DIRECTION('ref_axis',(1.,0.,0.));
#6592=DIRECTION('',(0.707106781186547,0.707106781186548,8.65956056235493E-17));
#6593=DIRECTION('center_axis',(0.,-1.,0.));
#6594=DIRECTION('ref_axis',(1.,0.,0.));
#6595=DIRECTION('center_axis',(0.,-1.,0.));
#6596=DIRECTION('ref_axis',(1.,0.,0.));
#6597=DIRECTION('',(0.,1.,0.));
#6598=DIRECTION('center_axis',(0.,1.,0.));
#6599=DIRECTION('ref_axis',(1.,0.,0.));
#6600=DIRECTION('center_axis',(0.,-1.,0.));
#6601=DIRECTION('ref_axis',(1.,0.,0.));
#6602=DIRECTION('',(-0.707106781186547,0.707106781186548,-8.65956056235493E-17));
#6603=DIRECTION('center_axis',(0.,-1.,0.));
#6604=DIRECTION('ref_axis',(0.,0.,-1.));
#6605=DIRECTION('center_axis',(0.,-1.,0.));
#6606=DIRECTION('ref_axis',(1.,0.,0.));
#6607=DIRECTION('center_axis',(0.,1.,0.));
#6608=DIRECTION('ref_axis',(1.,0.,0.));
#6609=DIRECTION('center_axis',(0.,1.,0.));
#6610=DIRECTION('ref_axis',(1.,0.,0.));
#6611=DIRECTION('',(-0.447213595499958,0.894427190999916,-5.47678698264203E-17));
#6612=DIRECTION('center_axis',(0.,-1.,0.));
#6613=DIRECTION('ref_axis',(1.,0.,0.));
#6614=DIRECTION('center_axis',(0.,1.,0.));
#6615=DIRECTION('ref_axis',(1.,0.,0.));
#6616=DIRECTION('',(0.,1.,0.));
#6617=DIRECTION('center_axis',(0.,1.,0.));
#6618=DIRECTION('ref_axis',(1.,0.,0.));
#6619=DIRECTION('center_axis',(0.,-1.,0.));
#6620=DIRECTION('ref_axis',(1.,0.,0.));
#6621=DIRECTION('',(-0.707106781186547,0.707106781186548,-8.65956056235493E-17));
#6622=DIRECTION('center_axis',(0.,-1.,0.));
#6623=DIRECTION('ref_axis',(0.,0.,-1.));
#6624=DIRECTION('center_axis',(0.866025403784439,0.,-0.5));
#6625=DIRECTION('ref_axis',(0.5,0.,0.866025403784439));
#6626=DIRECTION('',(-0.5,0.,-0.866025403784439));
#6627=DIRECTION('',(0.,-1.,0.));
#6628=DIRECTION('',(0.5,0.,0.866025403784439));
#6629=DIRECTION('',(0.,-1.,0.));
#6630=DIRECTION('center_axis',(1.60246890531964E-16,0.,-1.));
#6631=DIRECTION('ref_axis',(1.,0.,1.60246890531964E-16));
#6632=DIRECTION('',(-1.,0.,-1.60246890531964E-16));
#6633=DIRECTION('',(0.,-1.,0.));
#6634=DIRECTION('',(1.,0.,1.60246890531964E-16));
#6635=DIRECTION('center_axis',(-0.866025403784439,0.,-0.5));
#6636=DIRECTION('ref_axis',(0.5,0.,-0.866025403784439));
#6637=DIRECTION('',(-0.5,0.,0.866025403784439));
#6638=DIRECTION('',(0.,-1.,0.));
#6639=DIRECTION('',(0.5,0.,-0.866025403784439));
#6640=DIRECTION('center_axis',(-0.866025403784439,0.,0.5));
#6641=DIRECTION('ref_axis',(-0.5,0.,-0.866025403784439));
#6642=DIRECTION('',(0.5,0.,0.866025403784439));
#6643=DIRECTION('',(0.,-1.,0.));
#6644=DIRECTION('',(-0.5,0.,-0.866025403784439));
#6645=DIRECTION('center_axis',(-1.60246890531964E-16,0.,1.));
#6646=DIRECTION('ref_axis',(-1.,0.,-1.60246890531964E-16));
#6647=DIRECTION('',(1.,0.,1.60246890531964E-16));
#6648=DIRECTION('',(0.,-1.,0.));
#6649=DIRECTION('',(-1.,0.,-1.60246890531964E-16));
#6650=DIRECTION('center_axis',(0.866025403784439,0.,0.5));
#6651=DIRECTION('ref_axis',(-0.5,0.,0.866025403784439));
#6652=DIRECTION('',(0.5,0.,-0.866025403784439));
#6653=DIRECTION('',(-0.5,0.,0.866025403784439));
#6654=DIRECTION('center_axis',(0.,1.,0.));
#6655=DIRECTION('ref_axis',(1.,0.,0.));
#6656=DIRECTION('center_axis',(0.,-1.,0.));
#6657=DIRECTION('ref_axis',(0.,0.,-1.));
#8044=CARTESIAN_POINT('',(0.,0.,0.));
#8045=CARTESIAN_POINT('Origin',(0.3,0.4,0.));
#8046=CARTESIAN_POINT('',(-0.3,0.4,-3.67394039744206E-17));
#8047=CARTESIAN_POINT('Origin',(0.,0.4,0.));
#8048=CARTESIAN_POINT('Origin',(0.,0.375,0.));
#8049=CARTESIAN_POINT('',(-0.35,0.35,-4.28626379701573E-17));
#8050=CARTESIAN_POINT('Origin',(0.,0.35,0.));
#8051=CARTESIAN_POINT('',(-0.325,0.375,-3.9801020972289E-17));
#8052=CARTESIAN_POINT('Origin',(0.,0.19,0.));
#8053=CARTESIAN_POINT('',(-0.35,0.03,-4.28626379701574E-17));
#8054=CARTESIAN_POINT('Origin',(0.,0.03,0.));
#8055=CARTESIAN_POINT('',(-0.35,0.19,-4.28626379701574E-17));
#8056=CARTESIAN_POINT('Origin',(0.,0.0149999999999999,0.));
#8057=CARTESIAN_POINT('',(-0.32,-3.29597460435593E-17,-3.91886975727153E-17));
#8058=CARTESIAN_POINT('Origin',(0.,0.,0.));
#8059=CARTESIAN_POINT('',(-0.335,0.0149999999999999,-4.10256677714363E-17));
#8060=CARTESIAN_POINT('Origin',(0.22,0.,0.));
#8061=CARTESIAN_POINT('',(-0.22,-6.93889390390723E-18,-2.69422295812418E-17));
#8062=CARTESIAN_POINT('Origin',(0.,0.,0.));
#8063=CARTESIAN_POINT('Origin',(0.,-0.02,0.));
#8064=CARTESIAN_POINT('',(-0.1954,-0.0492,2.39295984553393E-17));
#8065=CARTESIAN_POINT('Origin',(0.,-0.0492,0.));
#8066=CARTESIAN_POINT('',(-0.21,-0.02,-2.57175827820944E-17));
#8067=CARTESIAN_POINT('Origin',(0.,-0.8,0.));
#8068=CARTESIAN_POINT('',(-0.1954,-1.5646,2.39295984553393E-17));
#8069=CARTESIAN_POINT('Origin',(0.,-1.5646,0.));
#8070=CARTESIAN_POINT('',(-0.1954,-0.8,-2.39295984553393E-17));
#8071=CARTESIAN_POINT('Origin',(0.,-1.58,0.));
#8072=CARTESIAN_POINT('',(-0.16,-1.6,-1.95943487863577E-17));
#8073=CARTESIAN_POINT('Origin',(0.,-1.6,0.));
#8074=CARTESIAN_POINT('',(-0.18,-1.58,-2.20436423846524E-17));
#8075=CARTESIAN_POINT('Origin',(0.,-1.6,0.));
#8076=CARTESIAN_POINT('Origin',(0.0866025403784439,-0.4,-0.15));
#8077=CARTESIAN_POINT('',(0.173205080756888,-0.4,0.));
#8078=CARTESIAN_POINT('',(0.0866025403784439,-0.4,-0.15));
#8079=CARTESIAN_POINT('',(0.173205080756888,-0.4,0.));
#8080=CARTESIAN_POINT('',(0.0866025403784439,-0.64,-0.15));
#8081=CARTESIAN_POINT('',(0.0866025403784439,-0.4,-0.15));
#8082=CARTESIAN_POINT('',(0.173205080756888,-0.64,0.));
#8083=CARTESIAN_POINT('',(0.173205080756888,-0.64,0.));
#8084=CARTESIAN_POINT('',(0.173205080756888,-0.4,0.));
#8085=CARTESIAN_POINT('Origin',(-0.0866025403784438,-0.4,-0.15));
#8086=CARTESIAN_POINT('',(-0.0866025403784438,-0.4,-0.15));
#8087=CARTESIAN_POINT('',(0.0866025403784439,-0.4,-0.15));
#8088=CARTESIAN_POINT('',(-0.0866025403784438,-0.64,-0.15));
#8089=CARTESIAN_POINT('',(-0.0866025403784438,-0.4,-0.15));
#8090=CARTESIAN_POINT('',(0.0866025403784439,-0.64,-0.15));
#8091=CARTESIAN_POINT('Origin',(-0.173205080756888,-0.4,-2.77555756156289E-17));
#8092=CARTESIAN_POINT('',(-0.173205080756888,-0.4,-2.12115047744981E-17));
#8093=CARTESIAN_POINT('',(-0.0866025403784438,-0.4,-0.15));
#8094=CARTESIAN_POINT('',(-0.173205080756888,-0.64,-2.77555756156289E-17));
#8095=CARTESIAN_POINT('',(-0.173205080756888,-0.4,-2.12115047744981E-17));
#8096=CARTESIAN_POINT('',(-0.0866025403784438,-0.64,-0.15));
#8097=CARTESIAN_POINT('Origin',(-0.0866025403784439,-0.4,0.15));
#8098=CARTESIAN_POINT('',(-0.0866025403784439,-0.4,0.15));
#8099=CARTESIAN_POINT('',(-0.173205080756888,-0.4,-2.12115047744981E-17));
#8100=CARTESIAN_POINT('',(-0.0866025403784439,-0.64,0.15));
#8101=CARTESIAN_POINT('',(-0.0866025403784439,-0.4,0.15));
#8102=CARTESIAN_POINT('',(-0.173205080756888,-0.64,-2.12115047744981E-17));
#8103=CARTESIAN_POINT('Origin',(0.0866025403784439,-0.4,0.15));
#8104=CARTESIAN_POINT('',(0.0866025403784439,-0.4,0.15));
#8105=CARTESIAN_POINT('',(-0.0866025403784439,-0.4,0.15));
#8106=CARTESIAN_POINT('',(0.0866025403784439,-0.64,0.15));
#8107=CARTESIAN_POINT('',(0.0866025403784439,-0.4,0.15));
#8108=CARTESIAN_POINT('',(-0.0866025403784439,-0.64,0.15));
#8109=CARTESIAN_POINT('Origin',(0.173205080756888,-0.4,0.));
#8110=CARTESIAN_POINT('',(0.0866025403784439,-0.4,0.15));
#8111=CARTESIAN_POINT('',(0.0866025403784439,-0.64,0.15));
#8112=CARTESIAN_POINT('Origin',(0.,-0.4,-2.77555756156289E-17));
#8113=CARTESIAN_POINT('Origin',(0.,-0.64,-2.77555756156289E-17));
#8239=UNCERTAINTY_MEASURE_WITH_UNIT(LENGTH_MEASURE(0.001),#8267,
'DISTANCE_ACCURACY_VALUE',
'Maximum model space distance between geometric entities at asserted c
onnectivities');
#8241=UNCERTAINTY_MEASURE_WITH_UNIT(LENGTH_MEASURE(0.001),#8267,
'DISTANCE_ACCURACY_VALUE',
'Maximum model space distance between geometric entities at asserted c
onnectivities');
#8264=(
GEOMETRIC_REPRESENTATION_CONTEXT(3)
GLOBAL_UNCERTAINTY_ASSIGNED_CONTEXT((#8239))
GLOBAL_UNIT_ASSIGNED_CONTEXT((#8267,#8269,#8270))
REPRESENTATION_CONTEXT('','3D')
);
#8266=(
GEOMETRIC_REPRESENTATION_CONTEXT(3)
GLOBAL_UNCERTAINTY_ASSIGNED_CONTEXT((#8241))
GLOBAL_UNIT_ASSIGNED_CONTEXT((#8267,#8269,#8270))
REPRESENTATION_CONTEXT('','3D')
);
#8267=(
LENGTH_UNIT()
NAMED_UNIT(*)
SI_UNIT(.CENTI.,.METRE.)
);
#8269=(
NAMED_UNIT(*)
PLANE_ANGLE_UNIT()
SI_UNIT($,.RADIAN.)
);
#8270=(
NAMED_UNIT(*)
SI_UNIT($,.STERADIAN.)
SOLID_ANGLE_UNIT()
);
#8293=SHAPE_DEFINITION_REPRESENTATION(#8319,#8380);
#8319=PRODUCT_DEFINITION_SHAPE('',$,#8405);
#8380=SHAPE_REPRESENTATION('',(#5295),#8264);
#8382=PRODUCT_DEFINITION_CONTEXT('part definition',#8456,'design');
#8405=PRODUCT_DEFINITION('Cap Screw - M4x16',
'Cap Screw - M4x16',#8429,#8382);
#8429=PRODUCT_DEFINITION_FORMATION('',$,#8480);
#8456=APPLICATION_CONTEXT(
'Core Data for Automotive Mechanical Design Process');
#8457=PRODUCT_CONTEXT('part definition',#8456,'mechanical');
#8480=PRODUCT('Cap Screw - M4x16','Cap Screw - M4x16',
'Cap Screw - M4x16',(#8457));
#8538=COLOUR_RGB('Black',0.12,0.14,0.17);
#8539=FILL_AREA_STYLE_COLOUR('',#8538);
#8540=FILL_AREA_STYLE('',(#8539));
#8541=SURFACE_STYLE_FILL_AREA(#8540);
#8542=SURFACE_SIDE_STYLE('',(#8541));
#8543=SURFACE_STYLE_USAGE(.BOTH.,#8542);
#8544=PRESENTATION_STYLE_ASSIGNMENT((#8543));
ENDSEC;
END-ISO-10303-21;
